ISO-10303-21;
HEADER;
/* Generated by software containing ST-Developer
 * from STEP Tools, Inc. (www.steptools.com) 
 */

FILE_DESCRIPTION(
/* description */ ('Quick-return (Whitworth) mechanism'),
/* implementation_level */ '2;1');

FILE_NAME(
/* name */ 'M4x4 collar screw.step',
/* time_stamp */ '2026-10-28T03:25:57-07:00',
/* author */ (''),
/* organization */ (''),
/* preprocessor_version */ 'ST-DEVELOPER v20.2',
/* originating_system */ 'Autodesk Translation Framework v15.17.0.0',
/* authorisation */ '');

FILE_SCHEMA (('AUTOMOTIVE_DESIGN { 1 0 10303 214 3 1 1 }'));
ENDSEC;

DATA;
#10=MECHANICAL_DESIGN_GEOMETRIC_PRESENTATION_REPRESENTATION('',(#527),#14878);
#357=CONICAL_SURFACE('',#9087,0.185,0.785398163397449);
#431=SHAPE_REPRESENTATION_RELATIONSHIP('SRR','None',#15102,#475);
#475=ADVANCED_BREP_SHAPE_REPRESENTATION('',(#578),#14859);
#527=STYLED_ITEM('',(#15413),#578);
#578=MANIFOLD_SOLID_BREP('Body1',#7882);
#746=FACE_BOUND('',#1995,.T.);
#939=PLANE('',#9076);
#940=PLANE('',#9078);
#941=PLANE('',#9079);
#942=PLANE('',#9080);
#943=PLANE('',#9081);
#944=PLANE('',#9082);
#945=PLANE('',#9083);
#946=PLANE('',#9084);
#947=PLANE('',#9085);
#1365=FACE_OUTER_BOUND('',#1986,.T.);
#1366=FACE_OUTER_BOUND('',#1987,.T.);
#1367=FACE_OUTER_BOUND('',#1988,.T.);
#1368=FACE_OUTER_BOUND('',#1989,.T.);
#1369=FACE_OUTER_BOUND('',#1990,.T.);
#1370=FACE_OUTER_BOUND('',#1991,.T.);
#1371=FACE_OUTER_BOUND('',#1992,.T.);
#1372=FACE_OUTER_BOUND('',#1993,.T.);
#1373=FACE_OUTER_BOUND('',#1994,.T.);
#1374=FACE_OUTER_BOUND('',#1996,.T.);
#1375=FACE_OUTER_BOUND('',#1997,.T.);
#1986=EDGE_LOOP('',(#6552));
#1987=EDGE_LOOP('',(#6553,#6554,#6555,#6556));
#1988=EDGE_LOOP('',(#6557,#6558,#6559,#6560));
#1989=EDGE_LOOP('',(#6561,#6562,#6563,#6564));
#1990=EDGE_LOOP('',(#6565,#6566,#6567,#6568));
#1991=EDGE_LOOP('',(#6569,#6570,#6571,#6572));
#1992=EDGE_LOOP('',(#6573,#6574,#6575,#6576));
#1993=EDGE_LOOP('',(#6577,#6578,#6579,#6580,#6581,#6582));
#1994=EDGE_LOOP('',(#6583));
#1995=EDGE_LOOP('',(#6584,#6585,#6586,#6587,#6588,#6589));
#1996=EDGE_LOOP('',(#6590,#6591,#6592,#6593));
#1997=EDGE_LOOP('',(#6594,#6595,#6596,#6597));
#2445=LINE('',#13991,#2968);
#2446=LINE('',#13993,#2969);
#2447=LINE('',#13995,#2970);
#2448=LINE('',#13996,#2971);
#2449=LINE('',#13999,#2972);
#2450=LINE('',#14001,#2973);
#2451=LINE('',#14002,#2974);
#2452=LINE('',#14005,#2975);
#2453=LINE('',#14007,#2976);
#2454=LINE('',#14008,#2977);
#2455=LINE('',#14011,#2978);
#2456=LINE('',#14013,#2979);
#2457=LINE('',#14014,#2980);
#2458=LINE('',#14017,#2981);
#2459=LINE('',#14019,#2982);
#2460=LINE('',#14020,#2983);
#2461=LINE('',#14022,#2984);
#2462=LINE('',#14023,#2985);
#2463=LINE('',#14031,#2986);
#2464=LINE('',#14033,#2987);
#2968=VECTOR('',#11062,1.);
#2969=VECTOR('',#11063,1.);
#2970=VECTOR('',#11064,1.);
#2971=VECTOR('',#11065,1.);
#2972=VECTOR('',#11068,1.);
#2973=VECTOR('',#11069,1.);
#2974=VECTOR('',#11070,1.);
#2975=VECTOR('',#11073,1.);
#2976=VECTOR('',#11074,1.);
#2977=VECTOR('',#11075,1.);
#2978=VECTOR('',#11078,1.);
#2979=VECTOR('',#11079,1.);
#2980=VECTOR('',#11080,1.);
#2981=VECTOR('',#11083,1.);
#2982=VECTOR('',#11084,1.);
#2983=VECTOR('',#11085,1.);
#2984=VECTOR('',#11088,1.);
#2985=VECTOR('',#11089,1.);
#2986=VECTOR('',#11100,0.185);
#2987=VECTOR('',#11103,0.2);
#3550=CIRCLE('',#9077,0.1954);
#3551=CIRCLE('',#9086,0.17);
#3552=CIRCLE('',#9088,0.1954);
#4071=VERTEX_POINT('',#13986);
#4072=VERTEX_POINT('',#13989);
#4073=VERTEX_POINT('',#13990);
#4074=VERTEX_POINT('',#13992);
#4075=VERTEX_POINT('',#13994);
#4076=VERTEX_POINT('',#13998);
#4077=VERTEX_POINT('',#14000);
#4078=VERTEX_POINT('',#14004);
#4079=VERTEX_POINT('',#14006);
#4080=VERTEX_POINT('',#14010);
#4081=VERTEX_POINT('',#14012);
#4082=VERTEX_POINT('',#14016);
#4083=VERTEX_POINT('',#14018);
#4084=VERTEX_POINT('',#14026);
#4085=VERTEX_POINT('',#14029);
#4933=EDGE_CURVE('',#4071,#4071,#3550,.T.);
#4934=EDGE_CURVE('',#4072,#4073,#2445,.T.);
#4935=EDGE_CURVE('',#4072,#4074,#2446,.T.);
#4936=EDGE_CURVE('',#4074,#4075,#2447,.T.);
#4937=EDGE_CURVE('',#4073,#4075,#2448,.T.);
#4938=EDGE_CURVE('',#4076,#4072,#2449,.T.);
#4939=EDGE_CURVE('',#4076,#4077,#2450,.T.);
#4940=EDGE_CURVE('',#4077,#4074,#2451,.T.);
#4941=EDGE_CURVE('',#4078,#4076,#2452,.T.);
#4942=EDGE_CURVE('',#4078,#4079,#2453,.T.);
#4943=EDGE_CURVE('',#4079,#4077,#2454,.T.);
#4944=EDGE_CURVE('',#4080,#4078,#2455,.T.);
#4945=EDGE_CURVE('',#4080,#4081,#2456,.T.);
#4946=EDGE_CURVE('',#4081,#4079,#2457,.T.);
#4947=EDGE_CURVE('',#4082,#4080,#2458,.T.);
#4948=EDGE_CURVE('',#4082,#4083,#2459,.T.);
#4949=EDGE_CURVE('',#4083,#4081,#2460,.T.);
#4950=EDGE_CURVE('',#4073,#4082,#2461,.T.);
#4951=EDGE_CURVE('',#4075,#4083,#2462,.T.);
#4952=EDGE_CURVE('',#4084,#4084,#3551,.T.);
#4953=EDGE_CURVE('',#4085,#4085,#3552,.T.);
#4954=EDGE_CURVE('',#4085,#4084,#2463,.T.);
#4955=EDGE_CURVE('',#4071,#4085,#2464,.T.);
#6552=ORIENTED_EDGE('',*,*,#4933,.F.);
#6553=ORIENTED_EDGE('',*,*,#4934,.F.);
#6554=ORIENTED_EDGE('',*,*,#4935,.T.);
#6555=ORIENTED_EDGE('',*,*,#4936,.T.);
#6556=ORIENTED_EDGE('',*,*,#4937,.F.);
#6557=ORIENTED_EDGE('',*,*,#4938,.F.);
#6558=ORIENTED_EDGE('',*,*,#4939,.T.);
#6559=ORIENTED_EDGE('',*,*,#4940,.T.);
#6560=ORIENTED_EDGE('',*,*,#4935,.F.);
#6561=ORIENTED_EDGE('',*,*,#4941,.F.);
#6562=ORIENTED_EDGE('',*,*,#4942,.T.);
#6563=ORIENTED_EDGE('',*,*,#4943,.T.);
#6564=ORIENTED_EDGE('',*,*,#4939,.F.);
#6565=ORIENTED_EDGE('',*,*,#4944,.F.);
#6566=ORIENTED_EDGE('',*,*,#4945,.T.);
#6567=ORIENTED_EDGE('',*,*,#4946,.T.);
#6568=ORIENTED_EDGE('',*,*,#4942,.F.);
#6569=ORIENTED_EDGE('',*,*,#4947,.F.);
#6570=ORIENTED_EDGE('',*,*,#4948,.T.);
#6571=ORIENTED_EDGE('',*,*,#4949,.T.);
#6572=ORIENTED_EDGE('',*,*,#4945,.F.);
#6573=ORIENTED_EDGE('',*,*,#4950,.F.);
#6574=ORIENTED_EDGE('',*,*,#4937,.T.);
#6575=ORIENTED_EDGE('',*,*,#4951,.T.);
#6576=ORIENTED_EDGE('',*,*,#4948,.F.);
#6577=ORIENTED_EDGE('',*,*,#4951,.F.);
#6578=ORIENTED_EDGE('',*,*,#4936,.F.);
#6579=ORIENTED_EDGE('',*,*,#4940,.F.);
#6580=ORIENTED_EDGE('',*,*,#4943,.F.);
#6581=ORIENTED_EDGE('',*,*,#4946,.F.);
#6582=ORIENTED_EDGE('',*,*,#4949,.F.);
#6583=ORIENTED_EDGE('',*,*,#4952,.F.);
#6584=ORIENTED_EDGE('',*,*,#4934,.T.);
#6585=ORIENTED_EDGE('',*,*,#4950,.T.);
#6586=ORIENTED_EDGE('',*,*,#4947,.T.);
#6587=ORIENTED_EDGE('',*,*,#4944,.T.);
#6588=ORIENTED_EDGE('',*,*,#4941,.T.);
#6589=ORIENTED_EDGE('',*,*,#4938,.T.);
#6590=ORIENTED_EDGE('',*,*,#4953,.F.);
#6591=ORIENTED_EDGE('',*,*,#4954,.T.);
#6592=ORIENTED_EDGE('',*,*,#4952,.T.);
#6593=ORIENTED_EDGE('',*,*,#4954,.F.);
#6594=ORIENTED_EDGE('',*,*,#4933,.T.);
#6595=ORIENTED_EDGE('',*,*,#4955,.T.);
#6596=ORIENTED_EDGE('',*,*,#4953,.T.);
#6597=ORIENTED_EDGE('',*,*,#4955,.F.);
#7345=CYLINDRICAL_SURFACE('',#9089,0.1954);
#7696=ADVANCED_FACE('',(#1365),#939,.F.);
#7697=ADVANCED_FACE('',(#1366),#940,.F.);
#7698=ADVANCED_FACE('',(#1367),#941,.F.);
#7699=ADVANCED_FACE('',(#1368),#942,.F.);
#7700=ADVANCED_FACE('',(#1369),#943,.F.);
#7701=ADVANCED_FACE('',(#1370),#944,.F.);
#7702=ADVANCED_FACE('',(#1371),#945,.F.);
#7703=ADVANCED_FACE('',(#1372),#946,.F.);
#7704=ADVANCED_FACE('',(#1373,#746),#947,.T.);
#7705=ADVANCED_FACE('',(#1374),#357,.T.);
#7706=ADVANCED_FACE('',(#1375),#7345,.T.);
#7882=CLOSED_SHELL('',(#7696,#7697,#7698,#7699,#7700,#7701,#7702,#7703,
#7704,#7705,#7706));
#9075=AXIS2_PLACEMENT_3D('',#13984,#11054,#11055);
#9076=AXIS2_PLACEMENT_3D('',#13985,#11056,#11057);
#9077=AXIS2_PLACEMENT_3D('',#13987,#11058,#11059);
#9078=AXIS2_PLACEMENT_3D('',#13988,#11060,#11061);
#9079=AXIS2_PLACEMENT_3D('',#13997,#11066,#11067);
#9080=AXIS2_PLACEMENT_3D('',#14003,#11071,#11072);
#9081=AXIS2_PLACEMENT_3D('',#14009,#11076,#11077);
#9082=AXIS2_PLACEMENT_3D('',#14015,#11081,#11082);
#9083=AXIS2_PLACEMENT_3D('',#14021,#11086,#11087);
#9084=AXIS2_PLACEMENT_3D('',#14024,#11090,#11091);
#9085=AXIS2_PLACEMENT_3D('',#14025,#11092,#11093);
#9086=AXIS2_PLACEMENT_3D('',#14027,#11094,#11095);
#9087=AXIS2_PLACEMENT_3D('',#14028,#11096,#11097);
#9088=AXIS2_PLACEMENT_3D('',#14030,#11098,#11099);
#9089=AXIS2_PLACEMENT_3D('',#14032,#11101,#11102);
#11054=DIRECTION('axis',(0.,0.,1.));
#11055=DIRECTION('refdir',(1.,0.,0.));
#11056=DIRECTION('center_axis',(0.,1.,0.));
#11057=DIRECTION('ref_axis',(1.,0.,0.));
#11058=DIRECTION('center_axis',(0.,1.,0.));
#11059=DIRECTION('ref_axis',(1.,0.,0.));
#11060=DIRECTION('center_axis',(0.866025403784439,0.,-0.5));
#11061=DIRECTION('ref_axis',(0.5,0.,0.866025403784439));
#11062=DIRECTION('',(0.5,0.,0.866025403784439));
#11063=DIRECTION('',(0.,-1.,0.));
#11064=DIRECTION('',(0.5,0.,0.866025403784439));
#11065=DIRECTION('',(0.,-1.,0.));
#11066=DIRECTION('center_axis',(1.20185167898973E-16,0.,-1.));
#11067=DIRECTION('ref_axis',(1.,0.,1.20185167898973E-16));
#11068=DIRECTION('',(1.,0.,1.20185167898973E-16));
#11069=DIRECTION('',(0.,-1.,0.));
#11070=DIRECTION('',(1.,0.,1.20185167898973E-16));
#11071=DIRECTION('center_axis',(-0.866025403784439,0.,-0.5));
#11072=DIRECTION('ref_axis',(0.5,0.,-0.866025403784439));
#11073=DIRECTION('',(0.5,0.,-0.866025403784439));
#11074=DIRECTION('',(0.,-1.,0.));
#11075=DIRECTION('',(0.5,0.,-0.866025403784439));
#11076=DIRECTION('center_axis',(-0.866025403784439,0.,0.5));
#11077=DIRECTION('ref_axis',(-0.5,0.,-0.866025403784439));
#11078=DIRECTION('',(-0.5,0.,-0.866025403784439));
#11079=DIRECTION('',(0.,-1.,0.));
#11080=DIRECTION('',(-0.5,0.,-0.866025403784439));
#11081=DIRECTION('center_axis',(-2.40370335797945E-16,0.,1.));
#11082=DIRECTION('ref_axis',(-1.,0.,-2.40370335797945E-16));
#11083=DIRECTION('',(-1.,0.,-2.40370335797945E-16));
#11084=DIRECTION('',(0.,-1.,0.));
#11085=DIRECTION('',(-1.,0.,-2.40370335797945E-16));
#11086=DIRECTION('center_axis',(0.866025403784439,0.,0.5));
#11087=DIRECTION('ref_axis',(-0.5,0.,0.866025403784439));
#11088=DIRECTION('',(-0.5,0.,0.866025403784439));
#11089=DIRECTION('',(-0.5,0.,0.866025403784439));
#11090=DIRECTION('center_axis',(0.,-1.,0.));
#11091=DIRECTION('ref_axis',(0.,0.,-1.));
#11092=DIRECTION('center_axis',(0.,1.,0.));
#11093=DIRECTION('ref_axis',(0.,0.,1.));
#11094=DIRECTION('center_axis',(0.,-1.,0.));
#11095=DIRECTION('ref_axis',(1.,0.,0.));
#11096=DIRECTION('center_axis',(0.,-1.,0.));
#11097=DIRECTION('ref_axis',(1.,0.,0.));
#11098=DIRECTION('center_axis',(0.,-1.,0.));
#11099=DIRECTION('ref_axis',(1.,0.,0.));
#11100=DIRECTION('',(0.707106781186548,0.707106781186547,8.65956056235494E-17));
#11101=DIRECTION('center_axis',(0.,-1.,0.));
#11102=DIRECTION('ref_axis',(1.,0.,0.));
#11103=DIRECTION('',(0.,1.,0.));
#13984=CARTESIAN_POINT('',(0.,0.,0.));
#13985=CARTESIAN_POINT('Origin',(0.,-0.4,0.));
#13986=CARTESIAN_POINT('',(-0.1954,-0.4,2.39295984553393E-17));
#13987=CARTESIAN_POINT('Origin',(0.,-0.4,0.));
#13988=CARTESIAN_POINT('Origin',(0.0577350269189626,0.,-0.1));
#13989=CARTESIAN_POINT('',(0.0577350269189626,0.,-0.1));
#13990=CARTESIAN_POINT('',(0.115470053837925,0.,0.));
#13991=CARTESIAN_POINT('',(0.0934187836487032,0.,-0.0381939203391614));
#13992=CARTESIAN_POINT('',(0.0577350269189626,-0.2,-0.1));
#13993=CARTESIAN_POINT('',(0.0577350269189626,0.,-0.1));
#13994=CARTESIAN_POINT('',(0.115470053837925,-0.2,0.));
#13995=CARTESIAN_POINT('',(0.115470053837925,-0.2,0.));
#13996=CARTESIAN_POINT('',(0.115470053837925,0.,0.));
#13997=CARTESIAN_POINT('Origin',(-0.0577350269189626,0.,-0.1));
#13998=CARTESIAN_POINT('',(-0.0577350269189626,0.,-0.1));
#13999=CARTESIAN_POINT('',(0.0561324865405187,0.,-0.1));
#14000=CARTESIAN_POINT('',(-0.0577350269189626,-0.2,-0.1));
#14001=CARTESIAN_POINT('',(-0.0577350269189626,0.,-0.1));
#14002=CARTESIAN_POINT('',(0.0577350269189626,-0.2,-0.1));
#14003=CARTESIAN_POINT('Origin',(-0.115470053837925,0.,-1.38777878078145E-17));
#14004=CARTESIAN_POINT('',(-0.115470053837925,0.,-1.41410031829988E-17));
#14005=CARTESIAN_POINT('',(-0.0797862971081845,0.,-0.0618060796608387));
#14006=CARTESIAN_POINT('',(-0.115470053837925,-0.2,-1.38777878078145E-17));
#14007=CARTESIAN_POINT('',(-0.115470053837925,0.,-1.41410031829988E-17));
#14008=CARTESIAN_POINT('',(-0.0577350269189626,-0.2,-0.1));
#14009=CARTESIAN_POINT('Origin',(-0.0577350269189626,0.,0.1));
#14010=CARTESIAN_POINT('',(-0.0577350269189626,0.,0.1));
#14011=CARTESIAN_POINT('',(-0.0509187836487033,0.,0.111806079660839));
#14012=CARTESIAN_POINT('',(-0.0577350269189626,-0.2,0.1));
#14013=CARTESIAN_POINT('',(-0.0577350269189626,0.,0.1));
#14014=CARTESIAN_POINT('',(-0.115470053837925,-0.2,-1.41410031829988E-17));
#14015=CARTESIAN_POINT('Origin',(0.0577350269189626,0.,0.1));
#14016=CARTESIAN_POINT('',(0.0577350269189626,0.,0.1));
#14017=CARTESIAN_POINT('',(0.113867513459481,0.,0.1));
#14018=CARTESIAN_POINT('',(0.0577350269189626,-0.2,0.1));
#14019=CARTESIAN_POINT('',(0.0577350269189626,0.,0.1));
#14020=CARTESIAN_POINT('',(-0.0577350269189626,-0.2,0.1));
#14021=CARTESIAN_POINT('Origin',(0.115470053837925,0.,0.));
#14022=CARTESIAN_POINT('',(0.122286297108185,0.,-0.0118060796608386));
#14023=CARTESIAN_POINT('',(0.0577350269189626,-0.2,0.1));
#14024=CARTESIAN_POINT('Origin',(0.,-0.2,0.));
#14025=CARTESIAN_POINT('Origin',(0.17,0.,0.));
#14026=CARTESIAN_POINT('',(-0.17,-8.67361737988404E-18,-2.0818995585505E-17));
#14027=CARTESIAN_POINT('Origin',(0.,0.,0.));
#14028=CARTESIAN_POINT('Origin',(0.,-0.015,0.));
#14029=CARTESIAN_POINT('',(-0.1954,-0.0254,-2.39295984553393E-17));
#14030=CARTESIAN_POINT('Origin',(0.,-0.0254,0.));
#14031=CARTESIAN_POINT('',(-0.185,-0.015,-2.2655965784226E-17));
#14032=CARTESIAN_POINT('Origin',(0.,-0.2775,0.));
#14033=CARTESIAN_POINT('',(-0.1954,-0.2775,-2.39295984553393E-17));
#14805=UNCERTAINTY_MEASURE_WITH_UNIT(LENGTH_MEASURE(0.001),#14879,
'DISTANCE_ACCURACY_VALUE',
'Maximum model space distance between geometric entities at asserted c
onnectivities');
#14824=UNCERTAINTY_MEASURE_WITH_UNIT(LENGTH_MEASURE(0.001),#14879,
'DISTANCE_ACCURACY_VALUE',
'Maximum model space distance between geometric entities at asserted c
onnectivities');
#14859=(
GEOMETRIC_REPRESENTATION_CONTEXT(3)
GLOBAL_UNCERTAINTY_ASSIGNED_CONTEXT((#14805))
GLOBAL_UNIT_ASSIGNED_CONTEXT((#14879,#14881,#14882))
REPRESENTATION_CONTEXT('','3D')
);
#14878=(
GEOMETRIC_REPRESENTATION_CONTEXT(3)
GLOBAL_UNCERTAINTY_ASSIGNED_CONTEXT((#14824))
GLOBAL_UNIT_ASSIGNED_CONTEXT((#14879,#14881,#14882))
REPRESENTATION_CONTEXT('','3D')
);
#14879=(
LENGTH_UNIT()
NAMED_UNIT(*)
SI_UNIT(.CENTI.,.METRE.)
);
#14881=(
NAMED_UNIT(*)
PLANE_ANGLE_UNIT()
SI_UNIT($,.RADIAN.)
);
#14882=(
NAMED_UNIT(*)
SI_UNIT($,.STERADIAN.)
SOLID_ANGLE_UNIT()
);
#14917=SHAPE_DEFINITION_REPRESENTATION(#14975,#15102);
#14975=PRODUCT_DEFINITION_SHAPE('',$,#15156);
#15102=SHAPE_REPRESENTATION('',(#9075),#14859);
#15121=PRODUCT_DEFINITION_CONTEXT('part definition',#15282,'design');
#15156=PRODUCT_DEFINITION('M4x4 collar screw','M4x4 collar screw',#15209,
#15121);
#15209=PRODUCT_DEFINITION_FORMATION('',$,#15318);
#15282=APPLICATION_CONTEXT(
'Core Data for Automotive Mechanical Design Process');
#15283=PRODUCT_CONTEXT('part definition',#15282,'mechanical');
#15318=PRODUCT('M4x4 collar screw','M4x4 collar screw',
'M4x4 collar screw',(#15283));
#15407=COLOUR_RGB('Black',0.12,0.14,0.17);
#15408=FILL_AREA_STYLE_COLOUR('',#15407);
#15409=FILL_AREA_STYLE('',(#15408));
#15410=SURFACE_STYLE_FILL_AREA(#15409);
#15411=SURFACE_SIDE_STYLE('',(#15410));
#15412=SURFACE_STYLE_USAGE(.BOTH.,#15411);
#15413=PRESENTATION_STYLE_ASSIGNMENT((#15412));
ENDSEC;
END-ISO-10303-21;
